ISO-10303-21;
HEADER;
FILE_DESCRIPTION (('STEP AP214'),
    '1' );
FILE_NAME ('hex bolt gradeab_iso_ISO 4014 - M5 x 30 x 16-N.step',
    '2026-10-27T17:01:19',
    ( '' ),
    ( '' ),
    'SwSTEP 2.0',
    'SolidWorks 2026',
    '' );
FILE_SCHEMA (( 'AUTOMOTIVE_DESIGN' ));
ENDSEC;

DATA;
#3=ORIENTED_EDGE ( 'NONE', *, *, #2101, .F. ) ;
#15=EDGE_LOOP ( 'NONE', ( #6802, #6787, #9525 ) ) ;
#47=CYLINDRICAL_SURFACE ( 'NONE', #4191, 4.000000000000000000 ) ;
#67=ORIENTED_EDGE ( 'NONE', *, *, #6101, .T. ) ;
#98=PLANE ( 'NONE',  #9893 ) ;
#107=CARTESIAN_POINT ( 'NONE',  ( 0.3572655899081578768, -4.618802153516999631, -3.329030144205522754E-16 ) ) ;
#118=ORIENTED_EDGE ( 'NONE', *, *, #8596, .T. ) ;
#121=EDGE_CURVE ( 'NONE', #14270, #6163, #532, .T. ) ;
#174=ORIENTED_EDGE ( 'NONE', *, *, #7655, .T. ) ;
#179=DIRECTION ( 'NONE',  ( -1.000000000000000000, -0.000000000000000000, -0.000000000000000000 ) ) ;
#194=VECTOR ( 'NONE', #6776, 1000.000000000000000 ) ;
#211=EDGE_CURVE ( 'NONE', #1708, #13374, #7694, .T. ) ;
#234=ORIENTED_EDGE ( 'NONE', *, *, #11746, .T. ) ;
#240=EDGE_CURVE ( 'NONE', #4614, #6705, #3374, .T. ) ;
#252=PLANE ( 'NONE',  #3852 ) ;
#259=COLOUR_RGB ( '',1.000000000000000000, 0.9490196078431372140, 0.9098039215686274384 ) ;
#264=VERTEX_POINT ( 'NONE', #11962 ) ;
#276=ORIENTED_EDGE ( 'NONE', *, *, #2072, .F. ) ;
#295=CARTESIAN_POINT ( 'NONE',  ( 3.500000000000000000, 2.309401076758500704, -4.000000000000000000 ) ) ;
#308=ORIENTED_EDGE ( 'NONE', *, *, #14248, .F. ) ;
#321=EDGE_LOOP ( 'NONE', ( #9410, #8500, #10695 ) ) ;
#335=DIRECTION ( 'NONE',  ( -1.000000000000000000, -0.000000000000000000, -0.000000000000000000 ) ) ;
#346=CARTESIAN_POINT ( 'NONE',  ( 0.1391502195351337900, -4.241015250120798719, 0.6543461111163306754 ) ) ;
#354=DIRECTION ( 'NONE',  ( -0.000000000000000000, 0.5000000000000014433, 0.8660254037844378194 ) ) ;
#377=ORIENTED_EDGE ( 'NONE', *, *, #14177, .F. ) ;
#409=ORIENTED_EDGE ( 'NONE', *, *, #121, .F. ) ;
#412=CARTESIAN_POINT ( 'NONE',  ( 3.500000000000000000, 4.618802153517012954, 0.000000000000000000 ) ) ;
#420=VECTOR ( 'NONE', #354, 1000.000000000000114 ) ;
#424=( NAMED_UNIT ( * ) SI_UNIT ( $, .STERADIAN. ) SOLID_ANGLE_UNIT ( ) );
#434=PRODUCT_DEFINITION_CONTEXT ( 'detailed design', #10077, 'design' ) ;
#468=AXIS2_PLACEMENT_3D ( 'NONE', #12874, #11750, #5944 ) ;
#475=AXIS2_PLACEMENT_3D ( 'NONE', #9476, #9545, #13980 ) ;
#479=VECTOR ( 'NONE', #13080, 999.9999999999998863 ) ;
#496=EDGE_LOOP ( 'NONE', ( #8869, #13118, #1381, #11688, #8994, #12958 ) ) ;
#522=FACE_OUTER_BOUND ( 'NONE', #10112, .T. ) ;
#532=LINE ( 'NONE', #10573, #7383 ) ;
#543=CARTESIAN_POINT ( 'NONE',  ( 2.999999999999999112, 4.000000000000000000, 0.000000000000000000 ) ) ;
#545=DIRECTION ( 'NONE',  ( 0.000000000000000000, 0.000000000000000000, -1.000000000000000000 ) ) ;
#563=CARTESIAN_POINT ( 'NONE',  ( 0.3572655899081607078, 2.309401076758500704, -4.000000000000000000 ) ) ;
#574=FACE_OUTER_BOUND ( 'NONE', #2465, .T. ) ;
#585=ORIENTED_EDGE ( 'NONE', *, *, #14248, .T. ) ;
#651=STYLED_ITEM('',(#14681),#2645);
#654=DIRECTION ( 'NONE',  ( 0.000000000000000000, 0.000000000000000000, -1.000000000000000000 ) ) ;
#684=FACE_OUTER_BOUND ( 'NONE', #2603, .T. ) ;
#699=ADVANCED_FACE ( 'NONE', ( #3178 ), #5256, .F. ) ;
#705=CIRCLE ( 'NONE', #7542, 2.500000000000000444 ) ;
#709=CIRCLE ( 'NONE', #9449, 4.000000000000000000 ) ;
#714=AXIS2_PLACEMENT_3D ( 'NONE', #6013, #14003, #4109 ) ;
#726=VECTOR ( 'NONE', #179, 1000.000000000000000 ) ;
#734=VERTEX_POINT ( 'NONE', #1989 ) ;
#744=ADVANCED_FACE ( 'NONE', ( #945 ), #5383, .F. ) ;
#768=ORIENTED_EDGE ( 'NONE', *, *, #9766, .F. ) ;
#808=VERTEX_POINT ( 'NONE', #6648 ) ;
#844=DIRECTION ( 'NONE',  ( -1.000000000000000000, -0.000000000000000000, -0.000000000000000000 ) ) ;
#853=EDGE_CURVE ( 'NONE', #5738, #1327, #12539, .T. ) ;
#882=FACE_BOUND ( 'NONE', #5683, .T. ) ;
#892=CARTESIAN_POINT ( 'NONE',  ( 0.1578711657514495215, -1.548887424847058769, 3.999999999999999112 ) ) ;
#920=VECTOR ( 'NONE', #11044, 1000.000000000000114 ) ;
#945=FACE_OUTER_BOUND ( 'NONE', #496, .T. ) ;
#1019=DIRECTION ( 'NONE',  ( 0.000000000000000000, 0.000000000000000000, 1.000000000000000000 ) ) ;
#1024=ORIENTED_EDGE ( 'NONE', *, *, #11359, .F. ) ;
#1034=DIRECTION ( 'NONE',  ( 0.000000000000000000, 1.000000000000000000, -0.000000000000000000 ) ) ;
#1043=ORIENTED_EDGE ( 'NONE', *, *, #7655, .F. ) ;
#1059=VERTEX_POINT ( 'NONE', #13258 ) ;
#1091=DIRECTION ( 'NONE',  ( 1.000000000000000000, 0.000000000000000000, -0.000000000000000000 ) ) ;
#1130=AXIS2_PLACEMENT_3D ( 'NONE', #14176, #6265, #9591 ) ;
#1148=FACE_OUTER_BOUND ( 'NONE', #13299, .T. ) ;
#1169=CARTESIAN_POINT ( 'NONE',  ( 3.500000000000000000, 0.000000000000000000, 0.000000000000000000 ) ) ;
#1179=AXIS2_PLACEMENT_3D ( 'NONE', #9634, #2921, #1797 ) ;
#1199=CARTESIAN_POINT ( 'NONE',  ( 2.999999999999999112, 0.000000000000000000, 0.000000000000000000 ) ) ;
#1243=EDGE_CURVE ( 'NONE', #13718, #4881, #11032, .T. ) ;
#1248=EDGE_CURVE ( 'NONE', #4325, #1327, #12801, .T. ) ;
#1259=ORIENTED_EDGE ( 'NONE', *, *, #5103, .T. ) ;
#1275=ORIENTED_EDGE ( 'NONE', *, *, #3249, .T. ) ;
#1293=DIRECTION ( 'NONE',  ( 0.000000000000000000, -0.5000000000000018874, -0.8660254037844375974 ) ) ;
#1315=EDGE_CURVE ( 'NONE', #1059, #2855, #4916, .T. ) ;
#1327=VERTEX_POINT ( 'NONE', #3808 ) ;
#1365=DIRECTION ( 'NONE',  ( 0.000000000000000000, 0.000000000000000000, -1.000000000000000000 ) ) ;
#1381=ORIENTED_EDGE ( 'NONE', *, *, #11454, .F. ) ;
#1401=CARTESIAN_POINT ( 'NONE',  ( 0.3572655899081578768, -4.618802153516999631, -3.329030144205522754E-16 ) ) ;
#1406=CARTESIAN_POINT ( 'NONE',  ( -2.267930716273388369E-15, 0.3911686820828841893, 3.999999999999995559 ) ) ;
#1473=FACE_OUTER_BOUND ( 'NONE', #9867, .T. ) ;
#1486=AXIS2_PLACEMENT_3D ( 'NONE', #5292, #3150, #10961 ) ;
#1495=ORIENTED_EDGE ( 'NONE', *, *, #12220, .T. ) ;
#1510=EDGE_CURVE ( 'NONE', #6705, #5856, #11501, .T. ) ;
#1533=ORIENTED_EDGE ( 'NONE', *, *, #1248, .F. ) ;
#1549=DIRECTION ( 'NONE',  ( -0.000000000000000000, 0.5000000000000014433, 0.8660254037844378194 ) ) ;
#1574=AXIS2_PLACEMENT_3D ( 'NONE', #7528, #7611, #4142 ) ;
#1578=CONICAL_SURFACE ( 'NONE', #7238, 4.000000000000000000, 1.047197551196600296 ) ;
#1620=DIRECTION ( 'NONE',  ( -1.000000000000000000, -0.000000000000000000, -0.000000000000000000 ) ) ;
#1625=DIRECTION ( 'NONE',  ( 0.000000000000000000, 0.000000000000000000, -1.000000000000000000 ) ) ;
#1657=PLANE ( 'NONE',  #7337 ) ;
#1659=AXIS2_PLACEMENT_3D ( 'NONE', #12812, #3819, #545 ) ;
#1688=B_SPLINE_CURVE_WITH_KNOTS ( 'NONE', 3,
 ( #6289, #13426, #3240, #12232, #2123, #4097 ),
 .UNSPECIFIED., .F., .F.,
 ( 4, 2, 4 ),
 ( 0.01237452868098001986, 0.01354396209252427784, 0.01471339550406853582 ),
 .UNSPECIFIED. ) ;
#1693=ORIENTED_EDGE ( 'NONE', *, *, #9766, .T. ) ;
#1699=( NAMED_UNIT ( * ) PLANE_ANGLE_UNIT ( ) SI_UNIT ( $, .RADIAN. ) );
#1708=VERTEX_POINT ( 'NONE', #10205 ) ;
#1723=ADVANCED_FACE ( 'NONE', ( #12779 ), #9600, .T. ) ;
#1727=DIRECTION ( 'NONE',  ( 0.000000000000000000, 0.000000000000000000, -1.000000000000000000 ) ) ;
#1749=CARTESIAN_POINT ( 'NONE',  ( 0.000000000000000000, 3.464101615137751278, -2.000000000000006217 ) ) ;
#1758=VERTEX_POINT ( 'NONE', #14040 ) ;
#1771=CARTESIAN_POINT ( 'NONE',  ( 3.700000000000000178, 0.000000000000000000, 0.000000000000000000 ) ) ;
#1779=APPLICATION_CONTEXT ( 'automotive_design' ) ;
#1786=CYLINDRICAL_SURFACE ( 'NONE', #6427, 4.000000000000000000 ) ;
#1797=DIRECTION ( 'NONE',  ( 0.000000000000000000, 0.000000000000000000, -1.000000000000000000 ) ) ;
#1864=SHAPE_REPRESENTATION_RELATIONSHIP ( 'NONE' , 'NONE' ,  #5462, #13030 ) ;
#1943=CARTESIAN_POINT ( 'NONE',  ( 2.999999999999999112, 2.309401076758500704, -4.000000000000000000 ) ) ;
#1959=ADVANCED_FACE ( 'NONE', ( #8571 ), #1578, .T. ) ;
#1989=CARTESIAN_POINT ( 'NONE',  ( 2.999999999999999112, -3.464101615137757051, -1.999999999999996669 ) ) ;
#2000=DIRECTION ( 'NONE',  ( -1.000000000000000000, -0.000000000000000000, -0.000000000000000000 ) ) ;
#2016=DIRECTION ( 'NONE',  ( -1.000000000000000000, -0.000000000000000000, -0.000000000000000000 ) ) ;
#2034=DIRECTION ( 'NONE',  ( 1.000000000000000000, 0.000000000000000000, -0.000000000000000000 ) ) ;
#2038=ORIENTED_EDGE ( 'NONE', *, *, #211, .T. ) ;
#2059=CARTESIAN_POINT ( 'NONE',  ( 2.999999999999999112, -4.618802153516999631, 0.000000000000000000 ) ) ;
#2072=EDGE_CURVE ( 'NONE', #2217, #12155, #10305, .T. ) ;
#2073=CARTESIAN_POINT ( 'NONE',  ( -2.222614453595284090E-15, -0.3908539631446481533, 3.999999999999996447 ) ) ;
#2074=ORIENTED_EDGE ( 'NONE', *, *, #10056, .F. ) ;
#2083=ADVANCED_FACE ( 'NONE', ( #10188 ), #47, .T. ) ;
#2101=EDGE_CURVE ( 'NONE', #5202, #734, #12179, .T. ) ;
#2120=CIRCLE ( 'NONE', #1659, 4.000000000000000000 ) ;
#2123=CARTESIAN_POINT ( 'NONE',  ( 1.863472483959459822E-17, 0.3911686820828793598, -4.000000000000000000 ) ) ;
#2129=CIRCLE ( 'NONE', #12989, 2.700000000000000622 ) ;
#2132=DIRECTION ( 'NONE',  ( 1.000000000000000000, 0.000000000000000000, 0.000000000000000000 ) ) ;
#2148=CARTESIAN_POINT ( 'NONE',  ( 33.50000000000000000, 0.000000000000000000, 2.054999999999999716 ) ) ;
#2169=FACE_OUTER_BOUND ( 'NONE', #5104, .T. ) ;
#2212=ADVANCED_FACE ( 'NONE', ( #12908 ), #7156, .F. ) ;
#2217=VERTEX_POINT ( 'NONE', #7442 ) ;
#2239=ORIENTED_EDGE ( 'NONE', *, *, #13792, .F. ) ;
#2283=ORIENTED_EDGE ( 'NONE', *, *, #8961, .F. ) ;
#2309=MECHANICAL_DESIGN_GEOMETRIC_PRESENTATION_REPRESENTATION('',(#651),#10568);
#2330=CARTESIAN_POINT ( 'NONE',  ( 0.03421028094653320167, 3.855830693249143515, 1.321505333908966184 ) ) ;
#2334=ORIENTED_EDGE ( 'NONE', *, *, #14098, .T. ) ;
#2338=B_SPLINE_CURVE_WITH_KNOTS ( 'NONE', 3,
 ( #13810, #1406, #9240, #10419, #10118, #8185 ),
 .UNSPECIFIED., .F., .F.,
 ( 4, 2, 4 ),
 ( 0.006655250997664721377, 0.007825277639709776745, 0.008995304281754830378 ),
 .UNSPECIFIED. ) ;
#2340=CARTESIAN_POINT ( 'NONE',  ( 2.999999999999999112, 0.000000000000000000, -4.000000000000000000 ) ) ;
#2374=B_SPLINE_CURVE_WITH_KNOTS ( 'NONE', 3,
 ( #11415, #8023, #2330, #9285, #10169, #11478 ),
 .UNSPECIFIED., .F., .F.,
 ( 4, 2, 4 ),
 ( 0.002336974151641533874, 0.003500975885716431542, 0.004664977619791329209 ),
 .UNSPECIFIED. ) ;
#2384=CIRCLE ( 'NONE', #12652, 2.054999999999999716 ) ;
#2388=ORIENTED_EDGE ( 'NONE', *, *, #211, .F. ) ;
#2417=ORIENTED_EDGE ( 'NONE', *, *, #1510, .F. ) ;
#2420=ORIENTED_EDGE ( 'NONE', *, *, #8101, .T. ) ;
#2426=LINE ( 'NONE', #9290, #726 ) ;
#2435=DIRECTION ( 'NONE',  ( -1.000000000000000000, -0.000000000000000000, -0.000000000000000000 ) ) ;
#2451=EDGE_LOOP ( 'NONE', ( #14230, #8899, #11648 ) ) ;
#2453=LINE ( 'NONE', #13895, #2762 ) ;
#2465=EDGE_LOOP ( 'NONE', ( #377, #5264, #7707, #6521, #7492, #14525 ) ) ;
#2473=DIRECTION ( 'NONE',  ( 1.000000000000000000, 0.000000000000000000, 0.000000000000000000 ) ) ;
#2544=VERTEX_POINT ( 'NONE', #4221 ) ;
#2554=FACE_OUTER_BOUND ( 'NONE', #10763, .T. ) ;
#2581=EDGE_CURVE ( 'NONE', #5903, #264, #13224, .T. ) ;
#2603=EDGE_LOOP ( 'NONE', ( #2074, #12432 ) ) ;
#2619=CARTESIAN_POINT ( 'NONE',  ( 2.999999999999999112, 3.464101615137752166, 2.000000000000003553 ) ) ;
#2623=AXIS2_PLACEMENT_3D ( 'NONE', #5030, #6040, #12767 ) ;
#2645=MANIFOLD_SOLID_BREP ( 'HeadFillet', #7861 ) ;
#2670=EDGE_CURVE ( 'NONE', #734, #5903, #14102, .T. ) ;
#2683=ADVANCED_FACE ( 'NONE', ( #574 ), #12843, .F. ) ;
#2722=DIRECTION ( 'NONE',  ( 1.000000000000000000, 0.000000000000000000, 0.000000000000000000 ) ) ;
#2728=FACE_OUTER_BOUND ( 'NONE', #2451, .T. ) ;
#2737=ORIENTED_EDGE ( 'NONE', *, *, #3249, .F. ) ;
#2751=CARTESIAN_POINT ( 'NONE',  ( 0.3572655899081558228, -2.309401076758485161, 3.999999999999999112 ) ) ;
#2762=VECTOR ( 'NONE', #12787, 1000.000000000000000 ) ;
#2766=VERTEX_POINT ( 'NONE', #5249 ) ;
#2797=VERTEX_POINT ( 'NONE', #7738 ) ;
#2806=AXIS2_PLACEMENT_3D ( 'NONE', #1771, #3997, #654 ) ;
#2818=DIRECTION ( 'NONE',  ( -1.000000000000000000, -0.000000000000000000, -0.000000000000000000 ) ) ;
#2830=CARTESIAN_POINT ( 'NONE',  ( 0.000000000000000000, 0.000000000000000000, 0.000000000000000000 ) ) ;
#2837=VERTEX_POINT ( 'NONE', #12092 ) ;
#2855=VERTEX_POINT ( 'NONE', #14308 ) ;
#2891=LINE ( 'NONE', #14181, #6391 ) ;
#2921=DIRECTION ( 'NONE',  ( 1.000000000000000000, 0.000000000000000000, -0.000000000000000000 ) ) ;
#2932=ORIENTED_EDGE ( 'NONE', *, *, #4778, .T. ) ;
#2970=CARTESIAN_POINT ( 'NONE',  ( 33.50000000000000000, 2.789133085058097101E-16, -2.054999999999999716 ) ) ;
#3040=CARTESIAN_POINT ( 'NONE',  ( 2.999999999999999112, 2.309401076758500704, -4.000000000000000000 ) ) ;
#3046=DIRECTION ( 'NONE',  ( -0.000000000000000000, 0.000000000000000000, -1.000000000000000000 ) ) ;
#3051=DIRECTION ( 'NONE',  ( -1.000000000000000000, -0.000000000000000000, -0.000000000000000000 ) ) ;
#3067=VECTOR ( 'NONE', #11534, 1000.000000000000000 ) ;
#3111=DIRECTION ( 'NONE',  ( 0.000000000000000000, 0.000000000000000000, -1.000000000000000000 ) ) ;
#3119=DIRECTION ( 'NONE',  ( 0.000000000000000000, -0.5000000000000018874, -0.8660254037844375974 ) ) ;
#3126=AXIS2_PLACEMENT_3D ( 'NONE', #7668, #2034, #5308 ) ;
#3130=DIRECTION ( 'NONE',  ( 0.000000000000000000, 0.000000000000000000, 1.000000000000000000 ) ) ;
#3150=DIRECTION ( 'NONE',  ( 1.000000000000000000, 0.000000000000000000, 0.000000000000000000 ) ) ;
#3165=CARTESIAN_POINT ( 'NONE',  ( 33.50000000000000000, 2.516649172247810568E-16, -2.054999999999999716 ) ) ;
#3178=FACE_OUTER_BOUND ( 'NONE', #11021, .T. ) ;
#3215=EDGE_LOOP ( 'NONE', ( #2239, #14185, #10089, #6748 ) ) ;
#3220=ADVANCED_FACE ( 'NONE', ( #5777 ), #4611, .T. ) ;
#3240=CARTESIAN_POINT ( 'NONE',  ( 0.1597025669806095838, 1.557591170363294975, -4.000000000000000000 ) ) ;
#3249=EDGE_CURVE ( 'NONE', #5903, #4614, #9654, .T. ) ;
#3300=ADVANCED_FACE ( 'NONE', ( #12267 ), #7281, .T. ) ;
#3315=EDGE_CURVE ( 'NONE', #734, #5738, #13462, .T. ) ;
#3357=CARTESIAN_POINT ( 'NONE',  ( 2.999999999999999112, -2.309401076758502480, -4.000000000000000000 ) ) ;
#3374=CIRCLE ( 'NONE', #5962, 4.000000000000000000 ) ;
#3400=EDGE_LOOP ( 'NONE', ( #13181, #11347, #12872 ) ) ;
#3463=CARTESIAN_POINT ( 'NONE',  ( 2.999999999999999112, 0.000000000000000000, 0.000000000000000000 ) ) ;
#3490=DIRECTION ( 'NONE',  ( -1.000000000000000000, -0.000000000000000000, -0.000000000000000000 ) ) ;
#3501=PLANE ( 'NONE',  #4563 ) ;
#3542=EDGE_LOOP ( 'NONE', ( #14226, #8608, #2334, #8662 ) ) ;
#3559=CARTESIAN_POINT ( 'NONE',  ( 0.3572655899081595976, 2.309401076758508253, 3.999999999999993339 ) ) ;
#3609=AXIS2_PLACEMENT_3D ( 'NONE', #14222, #9722, #6471 ) ;
#3624=DIRECTION ( 'NONE',  ( 0.000000000000000000, 0.000000000000000000, -1.000000000000000000 ) ) ;
#3647=EDGE_LOOP ( 'NONE', ( #67, #14255, #1275 ) ) ;
#3675=VERTEX_POINT ( 'NONE', #7971 ) ;
#3738=DIRECTION ( 'NONE',  ( 0.000000000000000000, 0.000000000000000000, 1.000000000000000000 ) ) ;
#3750=ORIENTED_EDGE ( 'NONE', *, *, #14606, .T. ) ;
#3763=ORIENTED_EDGE ( 'NONE', *, *, #7837, .T. ) ;
#3794=EDGE_LOOP ( 'NONE', ( #3763, #2932, #585 ) ) ;
#3796=B_SPLINE_CURVE_WITH_KNOTS ( 'NONE', 3,
 ( #14041, #10712, #14257, #8637, #11882, #7310 ),
 .UNSPECIFIED., .F., .F.,
 ( 4, 2, 4 ),
 ( 0.002336974151641558160, 0.003500975885716449323, 0.004664977619791340485 ),
 .UNSPECIFIED. ) ;
#3808=CARTESIAN_POINT ( 'NONE',  ( 0.3572655899080433572, -2.309401076758680116, -4.000000000000000000 ) ) ;
#3817=DIRECTION ( 'NONE',  ( -1.000000000000000000, -0.000000000000000000, -0.000000000000000000 ) ) ;
#3819=DIRECTION ( 'NONE',  ( 1.000000000000000000, 0.000000000000000000, -0.000000000000000000 ) ) ;
#3849=FACE_OUTER_BOUND ( 'NONE', #3647, .T. ) ;
#3852=AXIS2_PLACEMENT_3D ( 'NONE', #9203, #5800, #5583 ) ;
#3887=ORIENTED_EDGE ( 'NONE', *, *, #1315, .F. ) ;
#3947=CARTESIAN_POINT ( 'NONE',  ( 0.000000000000000000, 0.000000000000000000, 2.500000000000000444 ) ) ;
#3949=AXIS2_PLACEMENT_3D ( 'NONE', #1169, #1091, #4511 ) ;
#3977=LINE ( 'NONE', #412, #8975 ) ;
#3996=DIRECTION ( 'NONE',  ( 1.000000000000000000, 0.000000000000000000, 0.000000000000000000 ) ) ;
#3997=DIRECTION ( 'NONE',  ( 1.000000000000000000, 0.000000000000000000, -0.000000000000000000 ) ) ;
#4035=ORIENTED_EDGE ( 'NONE', *, *, #9352, .F. ) ;
#4044=CARTESIAN_POINT ( 'NONE',  ( 2.999999999999999112, -2.309401076758485605, 3.999999999999999112 ) ) ;
#4068=ORIENTED_EDGE ( 'NONE', *, *, #10181, .F. ) ;
#4096=DIRECTION ( 'NONE',  ( 0.000000000000000000, 0.000000000000000000, 1.000000000000000000 ) ) ;
#4097=CARTESIAN_POINT ( 'NONE',  ( 0.000000000000000000, 0.000000000000000000, -4.000000000000000000 ) ) ;
#4109=DIRECTION ( 'NONE',  ( -0.000000000000000000, 0.000000000000000000, 1.000000000000000000 ) ) ;
#4142=DIRECTION ( 'NONE',  ( -0.000000000000000000, 0.000000000000000000, -1.000000000000000000 ) ) ;
#4191=AXIS2_PLACEMENT_3D ( 'NONE', #12543, #2435, #9075 ) ;
#4221=CARTESIAN_POINT ( 'NONE',  ( 33.05499999999999972, 3.061616997868383634E-16, -2.500000000000000444 ) ) ;
#4259=VERTEX_POINT ( 'NONE', #563 ) ;
#4314=PRESENTATION_STYLE_ASSIGNMENT (( #5198 ) ) ;
#4325=VERTEX_POINT ( 'NONE', #6188 ) ;
#4344=LINE ( 'NONE', #3165, #920 ) ;
#4345=EDGE_CURVE ( 'NONE', #808, #1059, #7584, .T. ) ;
#4347=CARTESIAN_POINT ( 'NONE',  ( 0.000000000000000000, 0.000000000000000000, 0.000000000000000000 ) ) ;
#4352=VERTEX_POINT ( 'NONE', #9731 ) ;
#4401=DIRECTION ( 'NONE',  ( 1.000000000000000000, 0.000000000000000000, 0.000000000000000000 ) ) ;
#4482=FACE_OUTER_BOUND ( 'NONE', #13027, .T. ) ;
#4488=TOROIDAL_SURFACE ( 'NONE', #1179, 2.700000000000000622, 0.2000000000000000111 ) ;
#4492=ORIENTED_EDGE ( 'NONE', *, *, #2581, .F. ) ;
#4511=DIRECTION ( 'NONE',  ( 0.000000000000000000, 0.000000000000000000, -1.000000000000000000 ) ) ;
#4563=AXIS2_PLACEMENT_3D ( 'NONE', #9183, #9106, #11245 ) ;
#4611=CYLINDRICAL_SURFACE ( 'NONE', #14358, 2.500000000000000444 ) ;
#4614=VERTEX_POINT ( 'NONE', #13836 ) ;
#4626=ORIENTED_EDGE ( 'NONE', *, *, #5299, .T. ) ;
#4685=ADVANCED_FACE ( 'NONE', ( #684 ), #5209, .F. ) ;
#4730=CARTESIAN_POINT ( 'NONE',  ( 0.03421028094652913548, -3.855830693249139962, -1.321505333908958413 ) ) ;
#4743=( LENGTH_UNIT ( ) NAMED_UNIT ( * ) SI_UNIT ( .MILLI., .METRE. ) );
#4755=AXIS2_PLACEMENT_3D ( 'NONE', #6496, #7606, #8483 ) ;
#4778=EDGE_CURVE ( 'NONE', #2837, #13718, #2120, .T. ) ;
#4797=ORIENTED_EDGE ( 'NONE', *, *, #7269, .F. ) ;
#4820=DIRECTION ( 'NONE',  ( 0.000000000000000000, 0.000000000000000000, 1.000000000000000000 ) ) ;
#4826=LINE ( 'NONE', #7018, #9201 ) ;
#4831=ADVANCED_FACE ( 'NONE', ( #6171 ), #4488, .F. ) ;
#4881=VERTEX_POINT ( 'NONE', #12269 ) ;
#4908=CARTESIAN_POINT ( 'NONE',  ( 0.03363697881402896717, -0.7786124122131675707, -4.000000000000000000 ) ) ;
#4916=CIRCLE ( 'NONE', #7028, 4.000000000000000000 ) ;
#4921=ORIENTED_EDGE ( 'NONE', *, *, #9878, .F. ) ;
#4990=AXIS2_PLACEMENT_3D ( 'NONE', #13298, #7845, #3046 ) ;
#4994=ORIENTED_EDGE ( 'NONE', *, *, #8209, .F. ) ;
#5024=DIRECTION ( 'NONE',  ( 1.000000000000000000, 0.000000000000000000, 0.000000000000000000 ) ) ;
#5030=CARTESIAN_POINT ( 'NONE',  ( 3.700000000000000178, 3.306546357697854226E-16, 2.700000000000000622 ) ) ;
#5044=ADVANCED_FACE ( 'NONE', ( #2728 ), #13599, .T. ) ;
#5089=DIRECTION ( 'NONE',  ( -1.000000000000000000, -0.000000000000000000, -0.000000000000000000 ) ) ;
#5091=EDGE_CURVE ( 'NONE', #5856, #5202, #6852, .T. ) ;
#5103=EDGE_CURVE ( 'NONE', #2837, #2855, #13463, .T. ) ;
#5104=EDGE_LOOP ( 'NONE', ( #1693, #6603, #12360 ) ) ;
#5124=SURFACE_STYLE_FILL_AREA ( #8809 ) ;
#5151=AXIS2_PLACEMENT_3D ( 'NONE', #11966, #3051, #3130 ) ;
#5157=CARTESIAN_POINT ( 'NONE',  ( 33.50000000000000000, 0.000000000000000000, 0.000000000000000000 ) ) ;
#5169=DIRECTION ( 'NONE',  ( -1.000000000000000000, -0.000000000000000000, -0.000000000000000000 ) ) ;
#5195=CARTESIAN_POINT ( 'NONE',  ( 0.1578711657514692002, -1.548887424847152694, -4.000000000000000000 ) ) ;
#5198=SURFACE_STYLE_USAGE ( .BOTH. , #5413 ) ;
#5202=VERTEX_POINT ( 'NONE', #2340 ) ;
#5203=CIRCLE ( 'NONE', #475, 2.700000000000000622 ) ;
#5209=PLANE ( 'NONE',  #714 ) ;
#5249=CARTESIAN_POINT ( 'NONE',  ( 3.700000000000000178, 0.000000000000000000, 2.500000000000000444 ) ) ;
#5256=PLANE ( 'NONE',  #1574 ) ;
#5264=ORIENTED_EDGE ( 'NONE', *, *, #121, .T. ) ;
#5292=CARTESIAN_POINT ( 'NONE',  ( 0.000000000000000000, 0.000000000000000000, 0.000000000000000000 ) ) ;
#5299=EDGE_CURVE ( 'NONE', #13147, #12356, #2426, .T. ) ;
#5308=DIRECTION ( 'NONE',  ( 0.000000000000000000, 0.000000000000000000, -1.000000000000000000 ) ) ;
#5325=ORIENTED_EDGE ( 'NONE', *, *, #9990, .F. ) ;
#5328=LINE ( 'NONE', #3040, #10611 ) ;
#5333=UNCERTAINTY_MEASURE_WITH_UNIT (LENGTH_MEASURE( 1.000000000000000082E-05 ), #4743, 'distance_accuracy_value', 'NONE');
#5344=ORIENTED_EDGE ( 'NONE', *, *, #9527, .F. ) ;
#5383=PLANE ( 'NONE',  #10053 ) ;
#5404=PLANE ( 'NONE',  #4990 ) ;
#5406=CARTESIAN_POINT ( 'NONE',  ( 2.999999999999999112, 0.000000000000000000, 0.000000000000000000 ) ) ;
#5413=SURFACE_SIDE_STYLE ('',( #5124 ) ) ;
#5426=EDGE_CURVE ( 'NONE', #264, #734, #14017, .T. ) ;
#5462=SHAPE_REPRESENTATION ( 'hex bolt gradeab_iso_ISO 4014 - M5 x 30 x 16-N', ( #9440 ), #5943 ) ;
#5514=PLANE ( 'NONE',  #13461 ) ;
#5531=FACE_OUTER_BOUND ( 'NONE', #10622, .T. ) ;
#5532=CARTESIAN_POINT ( 'NONE',  ( 0.3572655899081558228, -2.309401076758485161, 3.999999999999999112 ) ) ;
#5583=DIRECTION ( 'NONE',  ( 1.000000000000000000, 0.000000000000000000, 0.000000000000000000 ) ) ;
#5593=AXIS2_PLACEMENT_3D ( 'NONE', #3463, #5817, #13573 ) ;
#5594=EDGE_CURVE ( 'NONE', #12155, #4614, #14585, .T. ) ;
#5679=CARTESIAN_POINT ( 'NONE',  ( 0.1586754815284836251, -4.240386000424027024, -0.6554360035617921021 ) ) ;
#5683=EDGE_LOOP ( 'NONE', ( #11116, #118 ) ) ;
#5684=CIRCLE ( 'NONE', #6164, 2.500000000000000444 ) ;
#5708=MECHANICAL_DESIGN_GEOMETRIC_PRESENTATION_REPRESENTATION('',(#8771),#10652);
#5709=DIRECTION ( 'NONE',  ( -1.000000000000000000, -0.000000000000000000, -0.000000000000000000 ) ) ;
#5711=CONICAL_SURFACE ( 'NONE', #9495, 4.000000000000000000, 1.047197551196600296 ) ;
#5727=ORIENTED_EDGE ( 'NONE', *, *, #7269, .T. ) ;
#5738=VERTEX_POINT ( 'NONE', #5795 ) ;
#5740=DIRECTION ( 'NONE',  ( 0.000000000000000000, 0.5000000000000018874, 0.8660254037844374864 ) ) ;
#5777=FACE_OUTER_BOUND ( 'NONE', #6392, .T. ) ;
#5795=CARTESIAN_POINT ( 'NONE',  ( 2.999999999999999112, -2.309401076758502480, -4.000000000000000000 ) ) ;
#5800=DIRECTION ( 'NONE',  ( -0.000000000000000000, 0.000000000000000000, 1.000000000000000000 ) ) ;
#5808=EDGE_CURVE ( 'NONE', #13276, #1708, #2384, .T. ) ;
#5817=DIRECTION ( 'NONE',  ( -1.000000000000000000, -0.000000000000000000, -0.000000000000000000 ) ) ;
#5856=VERTEX_POINT ( 'NONE', #11469 ) ;
#5860=ORIENTED_EDGE ( 'NONE', *, *, #4345, .T. ) ;
#5903=VERTEX_POINT ( 'NONE', #8223 ) ;
#5930=VECTOR ( 'NONE', #11701, 1000.000000000000114 ) ;
#5934=ORIENTED_EDGE ( 'NONE', *, *, #13940, .F. ) ;
#5943=( GEOMETRIC_REPRESENTATION_CONTEXT ( 3 ) GLOBAL_UNCERTAINTY_ASSIGNED_CONTEXT ( ( #10770 ) ) GLOBAL_UNIT_ASSIGNED_CONTEXT ( ( #7119, #13025, #7334 ) ) REPRESENTATION_CONTEXT ( 'NONE', 'WORKASPACE' ) );
#5944=DIRECTION ( 'NONE',  ( 0.000000000000000000, 0.000000000000000000, 1.000000000000000000 ) ) ;
#5962=AXIS2_PLACEMENT_3D ( 'NONE', #5406, #2000, #4096 ) ;
#5991=DIRECTION ( 'NONE',  ( 0.000000000000000000, 0.000000000000000000, 1.000000000000000000 ) ) ;
#6007=ORIENTED_EDGE ( 'NONE', *, *, #8101, .F. ) ;
#6013=CARTESIAN_POINT ( 'NONE',  ( 33.50000000000000000, 0.000000000000000000, 0.000000000000000000 ) ) ;
#6040=DIRECTION ( 'NONE',  ( -0.000000000000000000, 1.000000000000000000, -1.224646799147353207E-16 ) ) ;
#6101=EDGE_CURVE ( 'NONE', #4614, #13147, #2453, .T. ) ;
#6126=ORIENTED_EDGE ( 'NONE', *, *, #14606, .F. ) ;
#6134=AXIS2_PLACEMENT_3D ( 'NONE', #10219, #12350, #10141 ) ;
#6163=VERTEX_POINT ( 'NONE', #11412 ) ;
#6164=AXIS2_PLACEMENT_3D ( 'NONE', #8143, #12650, #7195 ) ;
#6171=FACE_OUTER_BOUND ( 'NONE', #3215, .T. ) ;
#6185=AXIS2_PLACEMENT_3D ( 'NONE', #8982, #2473, #1365 ) ;
#6188=CARTESIAN_POINT ( 'NONE',  ( 0.000000000000000000, 0.000000000000000000, -4.000000000000000000 ) ) ;
#6228=CARTESIAN_POINT ( 'NONE',  ( 0.000000000000000000, 0.000000000000000000, -4.000000000000000000 ) ) ;
#6265=DIRECTION ( 'NONE',  ( -1.000000000000000000, -0.000000000000000000, -0.000000000000000000 ) ) ;
#6286=EDGE_LOOP ( 'NONE', ( #6007, #12364, #10716, #2737, #8643, #3 ) ) ;
#6289=CARTESIAN_POINT ( 'NONE',  ( 0.3572655899081607078, 2.309401076758500704, -4.000000000000000000 ) ) ;
#6339=TOROIDAL_SURFACE ( 'NONE', #2806, 2.700000000000000622, 0.2000000000000000111 ) ;
#6391=VECTOR ( 'NONE', #1620, 1000.000000000000000 ) ;
#6392=EDGE_LOOP ( 'NONE', ( #13458, #11267, #234, #2283 ) ) ;
#6417=DIRECTION ( 'NONE',  ( 1.000000000000000000, 0.000000000000000000, 0.000000000000000000 ) ) ;
#6427=AXIS2_PLACEMENT_3D ( 'NONE', #10101, #13090, #1019 ) ;
#6471=DIRECTION ( 'NONE',  ( 0.000000000000000000, 0.000000000000000000, -1.000000000000000000 ) ) ;
#6496=CARTESIAN_POINT ( 'NONE',  ( 2.999999999999999112, 0.000000000000000000, 0.000000000000000000 ) ) ;
#6521=ORIENTED_EDGE ( 'NONE', *, *, #7837, .F. ) ;
#6539=ORIENTED_EDGE ( 'NONE', *, *, #5091, .F. ) ;
#6540=CARTESIAN_POINT ( 'NONE',  ( 0.000000000000000000, 0.000000000000000000, 0.000000000000000000 ) ) ;
#6569=AXIS2_PLACEMENT_3D ( 'NONE', #11716, #12912, #13128 ) ;
#6581=AXIS2_PLACEMENT_3D ( 'NONE', #12188, #14495, #6676 ) ;
#6599=DIRECTION ( 'NONE',  ( 0.000000000000000000, 0.000000000000000000, 1.000000000000000000 ) ) ;
#6603=ORIENTED_EDGE ( 'NONE', *, *, #1243, .T. ) ;
#6619=EDGE_LOOP ( 'NONE', ( #13805, #8843, #12462 ) ) ;
#6648=CARTESIAN_POINT ( 'NONE',  ( 0.3572655899081652042, 4.618802153517012066, 5.829523438926728986E-16 ) ) ;
#6676=DIRECTION ( 'NONE',  ( 0.000000000000000000, 0.000000000000000000, 1.000000000000000000 ) ) ;
#6705=VERTEX_POINT ( 'NONE', #2619 ) ;
#6748=ORIENTED_EDGE ( 'NONE', *, *, #14098, .F. ) ;
#6765=ORIENTED_EDGE ( 'NONE', *, *, #8744, .F. ) ;
#6776=DIRECTION ( 'NONE',  ( -1.000000000000000000, -0.000000000000000000, -0.000000000000000000 ) ) ;
#6787=ORIENTED_EDGE ( 'NONE', *, *, #14177, .T. ) ;
#6802=ORIENTED_EDGE ( 'NONE', *, *, #8209, .T. ) ;
#6805=CONICAL_SURFACE ( 'NONE', #11525, 4.000000000000000000, 1.047197551196600296 ) ;
#6852=CIRCLE ( 'NONE', #4755, 4.000000000000000000 ) ;
#6863=VERTEX_POINT ( 'NONE', #1943 ) ;
#6888=CARTESIAN_POINT ( 'NONE',  ( 0.000000000000000000, 0.000000000000000000, 0.000000000000000000 ) ) ;
#6944=CARTESIAN_POINT ( 'NONE',  ( 33.50000000000000000, 0.000000000000000000, 0.000000000000000000 ) ) ;
#6995=EDGE_CURVE ( 'NONE', #12155, #2217, #13639, .T. ) ;
#7018=CARTESIAN_POINT ( 'NONE',  ( 0.000000000000000000, 4.898587196589412829E-16, -4.000000000000000000 ) ) ;
#7028=AXIS2_PLACEMENT_3D ( 'NONE', #2830, #12940, #1727 ) ;
#7045=CARTESIAN_POINT ( 'NONE',  ( 33.50000000000000000, 0.000000000000000000, 0.000000000000000000 ) ) ;
#7054=DIRECTION ( 'NONE',  ( 0.000000000000000000, 0.8660254037844375974, -0.5000000000000019984 ) ) ;
#7119=( LENGTH_UNIT ( ) NAMED_UNIT ( * ) SI_UNIT ( .MILLI., .METRE. ) );
#7151=CARTESIAN_POINT ( 'NONE',  ( 0.000000000000000000, 0.000000000000000000, 0.000000000000000000 ) ) ;
#7156=PLANE ( 'NONE',  #9132 ) ;
#7185=ADVANCED_FACE ( 'NONE', ( #2554 ), #98, .F. ) ;
#7195=DIRECTION ( 'NONE',  ( 0.000000000000000000, 0.000000000000000000, 1.000000000000000000 ) ) ;
#7225=DIRECTION ( 'NONE',  ( 0.000000000000000000, 0.000000000000000000, -1.000000000000000000 ) ) ;
#7238=AXIS2_PLACEMENT_3D ( 'NONE', #7753, #13287, #3111 ) ;
#7254=CARTESIAN_POINT ( 'NONE',  ( 2.999999999999999112, 2.309401076758508253, 3.999999999999993339 ) ) ;
#7269=EDGE_CURVE ( 'NONE', #2855, #808, #2374, .T. ) ;
#7281=CONICAL_SURFACE ( 'NONE', #6581, 2.054999999999999716, 0.7853981633974482790 ) ;
#7289=FACE_OUTER_BOUND ( 'NONE', #3794, .T. ) ;
#7295=DIRECTION ( 'NONE',  ( 0.000000000000000000, -0.8660254037844381525, -0.5000000000000009992 ) ) ;
#7310=CARTESIAN_POINT ( 'NONE',  ( 0.3572655899081607078, 2.309401076758500704, -4.000000000000000000 ) ) ;
#7316=ORIENTED_EDGE ( 'NONE', *, *, #8403, .T. ) ;
#7334=( NAMED_UNIT ( * ) SI_UNIT ( $, .STERADIAN. ) SOLID_ANGLE_UNIT ( ) );
#7337=AXIS2_PLACEMENT_3D ( 'NONE', #543, #9494, #14001 ) ;
#7363=CARTESIAN_POINT ( 'NONE',  ( 0.3572655899081652042, 4.618802153517012066, 5.829523438926728986E-16 ) ) ;
#7377=ORIENTED_EDGE ( 'NONE', *, *, #8961, .T. ) ;
#7383=VECTOR ( 'NONE', #13989, 1000.000000000000000 ) ;
#7411=CARTESIAN_POINT ( 'NONE',  ( 0.3572655899080433572, -2.309401076758680116, -4.000000000000000000 ) ) ;
#7415=CARTESIAN_POINT ( 'NONE',  ( 0.000000000000000000, 5.258101095580073669E-15, 4.000000000000000000 ) ) ;
#7442=CARTESIAN_POINT ( 'NONE',  ( 3.500000000000000000, 4.898587196589412829E-16, -4.000000000000000000 ) ) ;
#7492=ORIENTED_EDGE ( 'NONE', *, *, #5299, .F. ) ;
#7496=AXIS2_PLACEMENT_3D ( 'NONE', #11896, #14204, #10796 ) ;
#7497=ORIENTED_EDGE ( 'NONE', *, *, #8850, .F. ) ;
#7528=CARTESIAN_POINT ( 'NONE',  ( 0.000000000000000000, 4.618802153517012954, 6.505213034913018715E-16 ) ) ;
#7542=AXIS2_PLACEMENT_3D ( 'NONE', #8149, #13930, #12739 ) ;
#7558=ORIENTED_EDGE ( 'NONE', *, *, #853, .T. ) ;
#7582=DIRECTION ( 'NONE',  ( 0.000000000000000000, 0.000000000000000000, -1.000000000000000000 ) ) ;
#7584=B_SPLINE_CURVE_WITH_KNOTS ( 'NONE', 3,
 ( #7363, #13054, #11857, #1749 ),
 .UNSPECIFIED., .F., .F.,
 ( 4, 4 ),
 ( 2.380737581619760596E-07, 0.002336974151641558160 ),
 .UNSPECIFIED. ) ;
#7605=CIRCLE ( 'NONE', #3126, 2.500000000000000444 ) ;
#7606=DIRECTION ( 'NONE',  ( -1.000000000000000000, -0.000000000000000000, -0.000000000000000000 ) ) ;
#7609=CARTESIAN_POINT ( 'NONE',  ( 3.500000000000000000, 0.000000000000000000, -2.700000000000000622 ) ) ;
#7611=DIRECTION ( 'NONE',  ( 1.000000000000000000, 0.000000000000000000, -0.000000000000000000 ) ) ;
#7618=VECTOR ( 'NONE', #13156, 1000.000000000000114 ) ;
#7655=EDGE_CURVE ( 'NONE', #2544, #13374, #13433, .T. ) ;
#7668=CARTESIAN_POINT ( 'NONE',  ( 3.700000000000000178, 0.000000000000000000, 0.000000000000000000 ) ) ;
#7694=LINE ( 'NONE', #2148, #7618 ) ;
#7697=CARTESIAN_POINT ( 'NONE',  ( 3.500000000000000000, 0.000000000000000000, 0.000000000000000000 ) ) ;
#7707=ORIENTED_EDGE ( 'NONE', *, *, #10009, .F. ) ;
#7719=DIRECTION ( 'NONE',  ( -1.000000000000000000, -0.000000000000000000, 0.000000000000000000 ) ) ;
#7738=CARTESIAN_POINT ( 'NONE',  ( 0.3572655899081578768, -4.618802153516999631, -3.329030144205522754E-16 ) ) ;
#7753=CARTESIAN_POINT ( 'NONE',  ( 0.000000000000000000, 0.000000000000000000, 0.000000000000000000 ) ) ;
#7754=FACE_OUTER_BOUND ( 'NONE', #13833, .T. ) ;
#7837=EDGE_CURVE ( 'NONE', #12356, #2837, #9758, .T. ) ;
#7845=DIRECTION ( 'NONE',  ( 1.000000000000000000, 0.000000000000000000, -0.000000000000000000 ) ) ;
#7846=EDGE_LOOP ( 'NONE', ( #1495, #7316, #10878 ) ) ;
#7861=CLOSED_SHELL ( 'NONE', ( #4831, #11356, #14544, #3220, #9967, #8090, #3300, #4685, #10916, #5044, #8919, #8566, #8713, #1723, #2083, #699, #13078, #12124, #11696, #13971, #12097, #1959, #11885, #744, #7185, #2683, #2212, #12288, #12831 ) ) ;
#7863=CARTESIAN_POINT ( 'NONE',  ( 2.999999999999999112, 4.000000000000000000, 0.000000000000000000 ) ) ;
#7867=DIRECTION ( 'NONE',  ( 0.000000000000000000, 0.000000000000000000, -1.000000000000000000 ) ) ;
#7923=DIRECTION ( 'NONE',  ( 1.000000000000000000, 0.000000000000000000, 0.000000000000000000 ) ) ;
#7971=CARTESIAN_POINT ( 'NONE',  ( 3.700000000000000178, 3.061616997868383634E-16, -2.500000000000000444 ) ) ;
#7990=ORIENTED_EDGE ( 'NONE', *, *, #13466, .F. ) ;
#8022=AXIS2_PLACEMENT_3D ( 'NONE', #5157, #5089, #8392 ) ;
#8023=CARTESIAN_POINT ( 'NONE',  ( -4.421511984667446784E-16, 3.660093687634854209, 1.660531772554310947 ) ) ;
#8075=CARTESIAN_POINT ( 'NONE',  ( 0.000000000000000000, -3.464101615137757051, -1.999999999999996225 ) ) ;
#8090=ADVANCED_FACE ( 'NONE', ( #522 ), #10345, .T. ) ;
#8101=EDGE_CURVE ( 'NONE', #2217, #5202, #4826, .T. ) ;
#8143=CARTESIAN_POINT ( 'NONE',  ( 33.05499999999999972, 0.000000000000000000, 0.000000000000000000 ) ) ;
#8149=CARTESIAN_POINT ( 'NONE',  ( 3.700000000000000178, 0.000000000000000000, 0.000000000000000000 ) ) ;
#8170=ORIENTED_EDGE ( 'NONE', *, *, #1243, .F. ) ;
#8185=CARTESIAN_POINT ( 'NONE',  ( 0.3572655899081595976, 2.309401076758508253, 3.999999999999993339 ) ) ;
#8209=EDGE_CURVE ( 'NONE', #6705, #14270, #14259, .T. ) ;
#8223=CARTESIAN_POINT ( 'NONE',  ( 2.999999999999999112, -3.464101615137750834, 2.000000000000007994 ) ) ;
#8330=PLANE ( 'NONE',  #10159 ) ;
#8334=B_SPLINE_CURVE_WITH_KNOTS ( 'NONE', 3,
 ( #1401, #346, #11583, #9236 ),
 .UNSPECIFIED., .F., .F.,
 ( 4, 4 ),
 ( 2.380737581620950413E-07, 0.002336974151641552089 ),
 .UNSPECIFIED. ) ;
#8392=DIRECTION ( 'NONE',  ( 0.000000000000000000, 0.000000000000000000, 1.000000000000000000 ) ) ;
#8403=EDGE_CURVE ( 'NONE', #4881, #4325, #709, .T. ) ;
#8483=DIRECTION ( 'NONE',  ( 0.000000000000000000, 0.000000000000000000, 1.000000000000000000 ) ) ;
#8491=ORIENTED_EDGE ( 'NONE', *, *, #9527, .T. ) ;
#8492=AXIS2_PLACEMENT_3D ( 'NONE', #9541, #10645, #5991 ) ;
#8500=ORIENTED_EDGE ( 'NONE', *, *, #11359, .T. ) ;
#8539=EDGE_CURVE ( 'NONE', #2766, #4352, #9695, .T. ) ;
#8566=ADVANCED_FACE ( 'NONE', ( #3849 ), #8330, .T. ) ;
#8571=FACE_OUTER_BOUND ( 'NONE', #7846, .T. ) ;
#8582=ORIENTED_EDGE ( 'NONE', *, *, #9878, .T. ) ;
#8585=CARTESIAN_POINT ( 'NONE',  ( 0.000000000000000000, -3.464101615137750834, 2.000000000000007994 ) ) ;
#8596=EDGE_CURVE ( 'NONE', #4352, #10367, #2129, .T. ) ;
#8608=ORIENTED_EDGE ( 'NONE', *, *, #11746, .F. ) ;
#8633=EDGE_CURVE ( 'NONE', #4325, #1059, #11095, .T. ) ;
#8637=CARTESIAN_POINT ( 'NONE',  ( 0.1586754815284860953, 2.687817229851475531, -3.344563996438206566 ) ) ;
#8643=ORIENTED_EDGE ( 'NONE', *, *, #2670, .F. ) ;
#8657=( NAMED_UNIT ( * ) SI_UNIT ( $, .STERADIAN. ) SOLID_ANGLE_UNIT ( ) );
#8662=ORIENTED_EDGE ( 'NONE', *, *, #8596, .F. ) ;
#8695=EDGE_LOOP ( 'NONE', ( #9762, #3750, #4797, #5325, #409, #4994 ) ) ;
#8703=CARTESIAN_POINT ( 'NONE',  ( 0.000000000000000000, 0.000000000000000000, 0.000000000000000000 ) ) ;
#8713=ADVANCED_FACE ( 'NONE', ( #10008 ), #5514, .T. ) ;
#8726=LINE ( 'NONE', #8939, #12021 ) ;
#8741=CIRCLE ( 'NONE', #13938, 2.054999999999999716 ) ;
#8744=EDGE_CURVE ( 'NONE', #13147, #5903, #10152, .T. ) ;
#8748=B_SPLINE_CURVE_WITH_KNOTS ( 'NONE', 3,
 ( #14612, #11827, #4730, #5679, #13567, #107 ),
 .UNSPECIFIED., .F., .F.,
 ( 4, 2, 4 ),
 ( 0.002336974151641552089, 0.003500975885716441950, 0.004664977619791332679 ),
 .UNSPECIFIED. ) ;
#8758=FACE_OUTER_BOUND ( 'NONE', #321, .T. ) ;
#8766=CARTESIAN_POINT ( 'NONE',  ( 3.500000000000000000, 0.000000000000000000, 0.000000000000000000 ) ) ;
#8771=STYLED_ITEM ( 'NONE', ( #4314 ), #13030 ) ;
#8789=DIRECTION ( 'NONE',  ( 0.000000000000000000, -0.4999999999999990563, 0.8660254037844391517 ) ) ;
#8809=FILL_AREA_STYLE ('',( #9624 ) ) ;
#8843=ORIENTED_EDGE ( 'NONE', *, *, #5426, .T. ) ;
#8850=EDGE_CURVE ( 'NONE', #13374, #2544, #5684, .T. ) ;
#8859=CARTESIAN_POINT ( 'NONE',  ( 0.000000000000000000, 0.000000000000000000, 0.000000000000000000 ) ) ;
#8869=ORIENTED_EDGE ( 'NONE', *, *, #5426, .F. ) ;
#8899=ORIENTED_EDGE ( 'NONE', *, *, #10343, .T. ) ;
#8910=EDGE_LOOP ( 'NONE', ( #12875, #12589, #13916, #13725, #6126, #4068 ) ) ;
#8919=ADVANCED_FACE ( 'NONE', ( #12877 ), #1657, .T. ) ;
#8929=DIRECTION ( 'NONE',  ( 1.000000000000000000, 0.000000000000000000, -0.000000000000000000 ) ) ;
#8939=CARTESIAN_POINT ( 'NONE',  ( 2.999999999999999112, 2.309401076758500704, -4.000000000000000000 ) ) ;
#8942=ORIENTED_EDGE ( 'NONE', *, *, #2072, .T. ) ;
#8950=ORIENTED_EDGE ( 'NONE', *, *, #6995, .T. ) ;
#8961=EDGE_CURVE ( 'NONE', #13374, #2766, #14062, .T. ) ;
#8962=CARTESIAN_POINT ( 'NONE',  ( 3.700000000000000178, 0.000000000000000000, -2.700000000000000622 ) ) ;
#8965=CARTESIAN_POINT ( 'NONE',  ( 0.1391502195351252413, -2.687187980154734923, -3.345653888883608040 ) ) ;
#8975=VECTOR ( 'NONE', #335, 1000.000000000000000 ) ;
#8979=VECTOR ( 'NONE', #1293, 999.9999999999998863 ) ;
#8982=CARTESIAN_POINT ( 'NONE',  ( 2.999999999999999112, 4.000000000000000000, 0.000000000000000000 ) ) ;
#8994=ORIENTED_EDGE ( 'NONE', *, *, #853, .F. ) ;
#9041=FACE_OUTER_BOUND ( 'NONE', #8910, .T. ) ;
#9056=CARTESIAN_POINT ( 'NONE',  ( 0.000000000000000000, -3.464101615137750834, 2.000000000000007994 ) ) ;
#9061=CARTESIAN_POINT ( 'NONE',  ( 3.500000000000000000, -4.618802153516999631, 0.000000000000000000 ) ) ;
#9075=DIRECTION ( 'NONE',  ( 0.000000000000000000, 0.000000000000000000, 1.000000000000000000 ) ) ;
#9106=DIRECTION ( 'NONE',  ( 0.000000000000000000, -0.8660254037844378194, 0.5000000000000014433 ) ) ;
#9132=AXIS2_PLACEMENT_3D ( 'NONE', #11644, #7295, #11790 ) ;
#9153=CARTESIAN_POINT ( 'NONE',  ( 0.000000000000000000, 3.464101615137752610, 2.000000000000003997 ) ) ;
#9183=CARTESIAN_POINT ( 'NONE',  ( 3.500000000000000000, 2.309401076758500704, -4.000000000000000000 ) ) ;
#9188=CARTESIAN_POINT ( 'NONE',  ( 2.999999999999999112, -4.618802153516999631, 0.000000000000000000 ) ) ;
#9201=VECTOR ( 'NONE', #9318, 1000.000000000000000 ) ;
#9203=CARTESIAN_POINT ( 'NONE',  ( 3.500000000000000000, 2.309401076758500704, -4.000000000000000000 ) ) ;
#9236=CARTESIAN_POINT ( 'NONE',  ( 0.000000000000000000, -3.464101615137750834, 2.000000000000007994 ) ) ;
#9240=CARTESIAN_POINT ( 'NONE',  ( 0.03458865240849798295, 0.7871057074736624859, 3.999999999999995559 ) ) ;
#9252=PRODUCT_DEFINITION_FORMATION_WITH_SPECIFIED_SOURCE ( 'ANY', '', #12393, .NOT_KNOWN. ) ;
#9275=DIRECTION ( 'NONE',  ( -1.000000000000000000, -0.000000000000000000, -0.000000000000000000 ) ) ;
#9285=CARTESIAN_POINT ( 'NONE',  ( 0.1586754815284889819, 4.240386000424035018, 0.6554360035617970981 ) ) ;
#9290=CARTESIAN_POINT ( 'NONE',  ( 3.500000000000000000, -2.309401076758485161, 3.999999999999999112 ) ) ;
#9311=CARTESIAN_POINT ( 'NONE',  ( -4.517043073611196936E-16, 3.070647092368435693, 2.681483223904233437 ) ) ;
#9318=DIRECTION ( 'NONE',  ( -1.000000000000000000, -0.000000000000000000, -0.000000000000000000 ) ) ;
#9338=ORIENTED_EDGE ( 'NONE', *, *, #1315, .T. ) ;
#9352=EDGE_CURVE ( 'NONE', #6863, #4259, #14111, .T. ) ;
#9380=LINE ( 'NONE', #13967, #14173 ) ;
#9410=ORIENTED_EDGE ( 'NONE', *, *, #12832, .T. ) ;
#9438=EDGE_CURVE ( 'NONE', #10367, #4352, #5203, .T. ) ;
#9440=AXIS2_PLACEMENT_3D ( 'NONE', #4347, #14302, #6417 ) ;
#9449=AXIS2_PLACEMENT_3D ( 'NONE', #8859, #8929, #13651 ) ;
#9476=CARTESIAN_POINT ( 'NONE',  ( 3.500000000000000000, 0.000000000000000000, 0.000000000000000000 ) ) ;
#9494=DIRECTION ( 'NONE',  ( 1.000000000000000000, 0.000000000000000000, 0.000000000000000000 ) ) ;
#9495=AXIS2_PLACEMENT_3D ( 'NONE', #7151, #5024, #9519 ) ;
#9519=DIRECTION ( 'NONE',  ( 0.000000000000000000, 0.000000000000000000, -1.000000000000000000 ) ) ;
#9525=ORIENTED_EDGE ( 'NONE', *, *, #240, .T. ) ;
#9527=EDGE_CURVE ( 'NONE', #5202, #6863, #5328, .T. ) ;
#9538=CARTESIAN_POINT ( 'NONE',  ( 2.999999999999999112, 2.309401076758500704, -4.000000000000000000 ) ) ;
#9541=CARTESIAN_POINT ( 'NONE',  ( 0.000000000000000000, 0.000000000000000000, 0.000000000000000000 ) ) ;
#9545=DIRECTION ( 'NONE',  ( -1.000000000000000000, -0.000000000000000000, 0.000000000000000000 ) ) ;
#9591=DIRECTION ( 'NONE',  ( 0.000000000000000000, 0.000000000000000000, 1.000000000000000000 ) ) ;
#9600=PLANE ( 'NONE',  #10570 ) ;
#9614=VECTOR ( 'NONE', #3119, 999.9999999999998863 ) ;
#9624=FILL_AREA_STYLE_COLOUR ( '', #259 ) ;
#9634=CARTESIAN_POINT ( 'NONE',  ( 3.700000000000000178, 0.000000000000000000, 0.000000000000000000 ) ) ;
#9654=CIRCLE ( 'NONE', #11749, 4.000000000000000000 ) ;
#9695=CIRCLE ( 'NONE', #2623, 0.2000000000000000944 ) ;
#9722=DIRECTION ( 'NONE',  ( 1.000000000000000000, 0.000000000000000000, 0.000000000000000000 ) ) ;
#9731=CARTESIAN_POINT ( 'NONE',  ( 3.500000000000000000, 3.306546357697854226E-16, 2.700000000000000622 ) ) ;
#9757=PRODUCT_CONTEXT ( 'NONE', #1779, 'mechanical' ) ;
#9758=B_SPLINE_CURVE_WITH_KNOTS ( 'NONE', 3,
 ( #12051, #11014, #892, #10950, #2073, #7415 ),
 .UNSPECIFIED., .F., .F.,
 ( 4, 2, 4 ),
 ( 0.004317080428420393828, 0.005486165713042557603, 0.006655250997664721377 ),
 .UNSPECIFIED. ) ;
#9762=ORIENTED_EDGE ( 'NONE', *, *, #10343, .F. ) ;
#9766=EDGE_CURVE ( 'NONE', #2797, #13718, #8334, .T. ) ;
#9793=DIRECTION ( 'NONE',  ( 1.000000000000000000, 0.000000000000000000, -0.000000000000000000 ) ) ;
#9851=LINE ( 'NONE', #12132, #9900 ) ;
#9867=EDGE_LOOP ( 'NONE', ( #10444, #14335, #7497, #2388 ) ) ;
#9878=EDGE_CURVE ( 'NONE', #5738, #5202, #8726, .T. ) ;
#9882=LINE ( 'NONE', #12020, #12035 ) ;
#9888=CARTESIAN_POINT ( 'NONE',  ( 3.500000000000000000, -2.309401076758502480, -4.000000000000000000 ) ) ;
#9893=AXIS2_PLACEMENT_3D ( 'NONE', #9061, #7054, #5740 ) ;
#9894=CARTESIAN_POINT ( 'NONE',  ( 2.999999999999999112, 4.618802153517012954, 0.000000000000000000 ) ) ;
#9900=VECTOR ( 'NONE', #2016, 1000.000000000000000 ) ;
#9903=FACE_OUTER_BOUND ( 'NONE', #10709, .T. ) ;
#9927=ORIENTED_EDGE ( 'NONE', *, *, #8633, .F. ) ;
#9967=ADVANCED_FACE ( 'NONE', ( #882, #9903 ), #5404, .T. ) ;
#9990=EDGE_CURVE ( 'NONE', #6163, #2855, #14322, .T. ) ;
#10008=FACE_OUTER_BOUND ( 'NONE', #6619, .T. ) ;
#10009=EDGE_CURVE ( 'NONE', #2837, #6163, #2338, .T. ) ;
#10053=AXIS2_PLACEMENT_3D ( 'NONE', #9888, #14393, #8789 ) ;
#10056=EDGE_CURVE ( 'NONE', #1708, #13276, #8741, .T. ) ;
#10066=CARTESIAN_POINT ( 'NONE',  ( 0.3572655899080433572, -2.309401076758680116, -4.000000000000000000 ) ) ;
#10077=APPLICATION_CONTEXT ( 'automotive_design' ) ;
#10089=ORIENTED_EDGE ( 'NONE', *, *, #9438, .F. ) ;
#10101=CARTESIAN_POINT ( 'NONE',  ( 0.000000000000000000, 0.000000000000000000, 0.000000000000000000 ) ) ;
#10112=EDGE_LOOP ( 'NONE', ( #5934, #174, #7377, #14117 ) ) ;
#10118=CARTESIAN_POINT ( 'NONE',  ( 0.2494252716035016415, 1.935831255942371154, 3.999999999999993339 ) ) ;
#10132=DIRECTION ( 'NONE',  ( 0.000000000000000000, 0.000000000000000000, 1.000000000000000000 ) ) ;
#10141=DIRECTION ( 'NONE',  ( 0.000000000000000000, 0.000000000000000000, -1.000000000000000000 ) ) ;
#10152=LINE ( 'NONE', #9188, #8979 ) ;
#10159=AXIS2_PLACEMENT_3D ( 'NONE', #12840, #2722, #7225 ) ;
#10169=CARTESIAN_POINT ( 'NONE',  ( 0.2484800633750021692, 4.430380094434247518, 0.3263565795980951090 ) ) ;
#10176=PRODUCT_DEFINITION_SHAPE ( 'NONE', 'NONE',  #12337 ) ;
#10181=EDGE_CURVE ( 'NONE', #5856, #1758, #9380, .T. ) ;
#10188=FACE_OUTER_BOUND ( 'NONE', #6286, .T. ) ;
#10205=CARTESIAN_POINT ( 'NONE',  ( 33.50000000000000000, 0.000000000000000000, 2.054999999999999716 ) ) ;
#10219=CARTESIAN_POINT ( 'NONE',  ( 0.000000000000000000, 0.000000000000000000, 0.000000000000000000 ) ) ;
#10230=EDGE_CURVE ( 'NONE', #264, #2797, #2891, .T. ) ;
#10262=ORIENTED_EDGE ( 'NONE', *, *, #240, .F. ) ;
#10305=CIRCLE ( 'NONE', #3949, 4.000000000000000000 ) ;
#10319=CARTESIAN_POINT ( 'NONE',  ( 3.500000000000000000, -2.309401076758502480, -4.000000000000000000 ) ) ;
#10343=EDGE_CURVE ( 'NONE', #1758, #6705, #9882, .T. ) ;
#10345=CYLINDRICAL_SURFACE ( 'NONE', #8492, 2.500000000000000444 ) ;
#10367=VERTEX_POINT ( 'NONE', #7609 ) ;
#10405=DIRECTION ( 'NONE',  ( 1.000000000000000000, 0.000000000000000000, -0.000000000000000000 ) ) ;
#10419=CARTESIAN_POINT ( 'NONE',  ( 0.1597025669806076964, 1.557591170363302080, 3.999999999999993339 ) ) ;
#10444=ORIENTED_EDGE ( 'NONE', *, *, #10056, .T. ) ;
#10449=CONICAL_SURFACE ( 'NONE', #1486, 4.000000000000000000, 1.047197551196600296 ) ;
#10497=ORIENTED_EDGE ( 'NONE', *, *, #5091, .T. ) ;
#10568=( GEOMETRIC_REPRESENTATION_CONTEXT ( 3 ) GLOBAL_UNCERTAINTY_ASSIGNED_CONTEXT ( ( #5333 ) ) GLOBAL_UNIT_ASSIGNED_CONTEXT ( ( #4743, #1699, #424 ) ) REPRESENTATION_CONTEXT ( 'NONE', 'WORKASPACE' ) );
#10570=AXIS2_PLACEMENT_3D ( 'NONE', #11592, #3996, #1625 ) ;
#10573=CARTESIAN_POINT ( 'NONE',  ( 3.500000000000000000, 2.309401076758508253, 3.999999999999993339 ) ) ;
#10583=VECTOR ( 'NONE', #12345, 1000.000000000000114 ) ;
#10611=VECTOR ( 'NONE', #10938, 1000.000000000000000 ) ;
#10622=EDGE_LOOP ( 'NONE', ( #276, #2420, #6539, #2417, #10262, #12626 ) ) ;
#10642=FACE_OUTER_BOUND ( 'NONE', #3542, .T. ) ;
#10645=DIRECTION ( 'NONE',  ( -1.000000000000000000, -0.000000000000000000, -0.000000000000000000 ) ) ;
#10652=( GEOMETRIC_REPRESENTATION_CONTEXT ( 3 ) GLOBAL_UNCERTAINTY_ASSIGNED_CONTEXT ( ( #14183 ) ) GLOBAL_UNIT_ASSIGNED_CONTEXT ( ( #13240, #10731, #8657 ) ) REPRESENTATION_CONTEXT ( 'NONE', 'WORKASPACE' ) );
#10659=CARTESIAN_POINT ( 'NONE',  ( 0.03421028094652456275, -3.072372537026353712, 2.678494666091038034 ) ) ;
#10680=CONICAL_SURFACE ( 'NONE', #3609, 4.000000000000000000, 1.047197551196600296 ) ;
#10695=ORIENTED_EDGE ( 'NONE', *, *, #8633, .T. ) ;
#10709=EDGE_LOOP ( 'NONE', ( #8950, #8942 ) ) ;
#10712=CARTESIAN_POINT ( 'NONE',  ( -1.528470953320384370E-15, 3.268109542640656784, -2.339468227445699711 ) ) ;
#10716=ORIENTED_EDGE ( 'NONE', *, *, #5594, .T. ) ;
#10731=( NAMED_UNIT ( * ) PLANE_ANGLE_UNIT ( ) SI_UNIT ( $, .RADIAN. ) );
#10763=EDGE_LOOP ( 'NONE', ( #6765, #4626, #308, #768, #13560, #4492 ) ) ;
#10770=UNCERTAINTY_MEASURE_WITH_UNIT (LENGTH_MEASURE( 1.000000000000000082E-05 ), #7119, 'distance_accuracy_value', 'NONE');
#10773=ORIENTED_EDGE ( 'NONE', *, *, #12796, .T. ) ;
#10796=DIRECTION ( 'NONE',  ( 0.000000000000000000, 0.000000000000000000, -1.000000000000000000 ) ) ;
#10825=AXIS2_PLACEMENT_3D ( 'NONE', #7697, #10405, #3624 ) ;
#10852=CIRCLE ( 'NONE', #14155, 0.2000000000000000944 ) ;
#10862=AXIS2_PLACEMENT_3D ( 'NONE', #7863, #7923, #12346 ) ;
#10877=CARTESIAN_POINT ( 'NONE',  ( 2.999999999999999112, 2.309401076758508253, 3.999999999999993339 ) ) ;
#10878=ORIENTED_EDGE ( 'NONE', *, *, #1248, .T. ) ;
#10899=FACE_OUTER_BOUND ( 'NONE', #3400, .T. ) ;
#10916=ADVANCED_FACE ( 'NONE', ( #4482 ), #12590, .T. ) ;
#10938=DIRECTION ( 'NONE',  ( 0.000000000000000000, 1.000000000000000000, -0.000000000000000000 ) ) ;
#10950=CARTESIAN_POINT ( 'NONE',  ( 0.03363697881402284012, -0.7786124122131168335, 3.999999999999997335 ) ) ;
#10961=DIRECTION ( 'NONE',  ( 0.000000000000000000, 0.000000000000000000, -1.000000000000000000 ) ) ;
#11014=CARTESIAN_POINT ( 'NONE',  ( 0.2486750293982080140, -1.933232340707284447, 3.999999999999998224 ) ) ;
#11021=EDGE_LOOP ( 'NONE', ( #9927, #12183, #8170, #13934, #1259, #3887 ) ) ;
#11032=CIRCLE ( 'NONE', #7496, 4.000000000000000000 ) ;
#11044=DIRECTION ( 'NONE',  ( -0.7071067811865474617, 8.659560562354932858E-17, -0.7071067811865474617 ) ) ;
#11095=CIRCLE ( 'NONE', #12266, 4.000000000000000000 ) ;
#11116=ORIENTED_EDGE ( 'NONE', *, *, #9438, .T. ) ;
#11140=CARTESIAN_POINT ( 'NONE',  ( 0.1586754815284800446, -2.687817229851461764, 3.344563996438204789 ) ) ;
#11142=EDGE_LOOP ( 'NONE', ( #7990, #14298, #2038, #1043 ) ) ;
#11144=DIRECTION ( 'NONE',  ( 0.000000000000000000, 0.000000000000000000, -1.000000000000000000 ) ) ;
#11145=SHAPE_DEFINITION_REPRESENTATION ( #10176, #5462 ) ;
#11171=B_SPLINE_CURVE_WITH_KNOTS ( 'NONE', 3,
 ( #10066, #8965, #11398, #8075 ),
 .UNSPECIFIED., .F., .F.,
 ( 4, 4 ),
 ( 2.380737582663283482E-07, 0.002336974151641552089 ),
 .UNSPECIFIED. ) ;
#11245=DIRECTION ( 'NONE',  ( 0.000000000000000000, -0.5000000000000014433, -0.8660254037844378194 ) ) ;
#11267=ORIENTED_EDGE ( 'NONE', *, *, #13940, .T. ) ;
#11317=CONICAL_SURFACE ( 'NONE', #8022, 2.054999999999999716, 0.7853981633974482790 ) ;
#11347=ORIENTED_EDGE ( 'NONE', *, *, #9990, .T. ) ;
#11356=ADVANCED_FACE ( 'NONE', ( #5531 ), #1786, .T. ) ;
#11359=EDGE_CURVE ( 'NONE', #4259, #4325, #1688, .T. ) ;
#11398=CARTESIAN_POINT ( 'NONE',  ( -4.407436607684889181E-15, -3.070647092368449016, -2.681483223904198354 ) ) ;
#11412=CARTESIAN_POINT ( 'NONE',  ( 0.3572655899081595976, 2.309401076758508253, 3.999999999999993339 ) ) ;
#11415=CARTESIAN_POINT ( 'NONE',  ( 0.000000000000000000, 3.464101615137752610, 2.000000000000003997 ) ) ;
#11454=EDGE_CURVE ( 'NONE', #4881, #2797, #8748, .T. ) ;
#11469=CARTESIAN_POINT ( 'NONE',  ( 2.999999999999999112, 3.464101615137751278, -2.000000000000005773 ) ) ;
#11478=CARTESIAN_POINT ( 'NONE',  ( 0.3572655899081652042, 4.618802153517012066, 5.829523438926728986E-16 ) ) ;
#11490=B_SPLINE_CURVE_WITH_KNOTS ( 'NONE', 3,
 ( #8585, #12314, #10659, #11140, #11828, #5532 ),
 .UNSPECIFIED., .F., .F.,
 ( 4, 2, 4 ),
 ( 0.002336974151641552089, 0.003500975885716447588, 0.004664977619791343087 ),
 .UNSPECIFIED. ) ;
#11501=CIRCLE ( 'NONE', #5151, 4.000000000000000000 ) ;
#11525=AXIS2_PLACEMENT_3D ( 'NONE', #12237, #2132, #11144 ) ;
#11534=DIRECTION ( 'NONE',  ( 0.000000000000000000, -1.000000000000000000, 1.314525273895018220E-15 ) ) ;
#11583=CARTESIAN_POINT ( 'NONE',  ( -8.838721003385150447E-15, -3.857556137907065974, 1.318516776095768339 ) ) ;
#11587=CARTESIAN_POINT ( 'NONE',  ( 0.1391502195351392857, 2.687187980154705613, 3.345653888883666660 ) ) ;
#11592=CARTESIAN_POINT ( 'NONE',  ( 2.999999999999999112, 4.000000000000000000, 0.000000000000000000 ) ) ;
#11644=CARTESIAN_POINT ( 'NONE',  ( 3.500000000000000000, 4.618802153517012954, 0.000000000000000000 ) ) ;
#11648=ORIENTED_EDGE ( 'NONE', *, *, #1510, .T. ) ;
#11688=ORIENTED_EDGE ( 'NONE', *, *, #12220, .F. ) ;
#11696=ADVANCED_FACE ( 'NONE', ( #7289 ), #5711, .T. ) ;
#11701=DIRECTION ( 'NONE',  ( 0.000000000000000000, 0.4999999999999990563, -0.8660254037844391517 ) ) ;
#11716=CARTESIAN_POINT ( 'NONE',  ( 3.500000000000000000, 2.309401076758508253, 3.999999999999993339 ) ) ;
#11746=EDGE_CURVE ( 'NONE', #3675, #2766, #7605, .T. ) ;
#11749=AXIS2_PLACEMENT_3D ( 'NONE', #1199, #5709, #6599 ) ;
#11750=DIRECTION ( 'NONE',  ( -1.000000000000000000, -0.000000000000000000, -0.000000000000000000 ) ) ;
#11790=DIRECTION ( 'NONE',  ( 0.000000000000000000, 0.5000000000000008882, -0.8660254037844380415 ) ) ;
#11827=CARTESIAN_POINT ( 'NONE',  ( -4.490121653395046097E-15, -3.660093687634849768, -1.660531772554302288 ) ) ;
#11828=CARTESIAN_POINT ( 'NONE',  ( 0.2484800633749931209, -2.497823135841249709, 3.673643420401906390 ) ) ;
#11829=CARTESIAN_POINT ( 'NONE',  ( 0.2486750293982372684, -1.933232340707399910, -4.000000000000000000 ) ) ;
#11857=CARTESIAN_POINT ( 'NONE',  ( -1.654100357141833219E-15, 3.857556137907077964, -1.318516776095772336 ) ) ;
#11882=CARTESIAN_POINT ( 'NONE',  ( 0.2484800633749985332, 2.497823135841265252, -3.673643420401908166 ) ) ;
#11885=ADVANCED_FACE ( 'NONE', ( #1148 ), #252, .F. ) ;
#11896=CARTESIAN_POINT ( 'NONE',  ( 0.000000000000000000, 0.000000000000000000, 0.000000000000000000 ) ) ;
#11962=CARTESIAN_POINT ( 'NONE',  ( 2.999999999999999112, -4.618802153516999631, 0.000000000000000000 ) ) ;
#11966=CARTESIAN_POINT ( 'NONE',  ( 2.999999999999999112, 0.000000000000000000, 0.000000000000000000 ) ) ;
#12020=CARTESIAN_POINT ( 'NONE',  ( 2.999999999999999112, 4.618802153517012954, 0.000000000000000000 ) ) ;
#12021=VECTOR ( 'NONE', #1034, 1000.000000000000000 ) ;
#12035=VECTOR ( 'NONE', #13423, 999.9999999999998863 ) ;
#12049=VECTOR ( 'NONE', #3817, 1000.000000000000000 ) ;
#12051=CARTESIAN_POINT ( 'NONE',  ( 0.3572655899081558228, -2.309401076758485161, 3.999999999999999112 ) ) ;
#12092=CARTESIAN_POINT ( 'NONE',  ( 0.000000000000000000, 5.258101095580073669E-15, 4.000000000000000000 ) ) ;
#12097=ADVANCED_FACE ( 'NONE', ( #8758 ), #10680, .T. ) ;
#12124=ADVANCED_FACE ( 'NONE', ( #10899 ), #10449, .T. ) ;
#12132=CARTESIAN_POINT ( 'NONE',  ( 0.000000000000000000, 3.061616997868383634E-16, -2.500000000000000444 ) ) ;
#12155=VERTEX_POINT ( 'NONE', #13322 ) ;
#12179=CIRCLE ( 'NONE', #5593, 4.000000000000000000 ) ;
#12183=ORIENTED_EDGE ( 'NONE', *, *, #8403, .F. ) ;
#12188=CARTESIAN_POINT ( 'NONE',  ( 33.50000000000000000, 0.000000000000000000, 0.000000000000000000 ) ) ;
#12220=EDGE_CURVE ( 'NONE', #1327, #4881, #11171, .T. ) ;
#12232=CARTESIAN_POINT ( 'NONE',  ( 0.03458865240850033523, 0.7871057074736559356, -4.000000000000000000 ) ) ;
#12237=CARTESIAN_POINT ( 'NONE',  ( 0.000000000000000000, 0.000000000000000000, 0.000000000000000000 ) ) ;
#12266=AXIS2_PLACEMENT_3D ( 'NONE', #6540, #9793, #14028 ) ;
#12267=FACE_OUTER_BOUND ( 'NONE', #11142, .T. ) ;
#12269=CARTESIAN_POINT ( 'NONE',  ( 0.000000000000000000, -3.464101615137757051, -1.999999999999996225 ) ) ;
#12288=ADVANCED_FACE ( 'NONE', ( #9041 ), #3501, .F. ) ;
#12292=CARTESIAN_POINT ( 'NONE',  ( 0.000000000000000000, 0.000000000000000000, 4.000000000000000000 ) ) ;
#12314=CARTESIAN_POINT ( 'NONE',  ( -9.018359789416532555E-15, -3.268109542640643905, 2.339468227445693937 ) ) ;
#12337=PRODUCT_DEFINITION ( 'UNKNOWN', '', #9252, #434 ) ;
#12345=DIRECTION ( 'NONE',  ( 0.000000000000000000, 0.4999999999999990563, -0.8660254037844391517 ) ) ;
#12346=DIRECTION ( 'NONE',  ( 0.000000000000000000, 0.000000000000000000, -1.000000000000000000 ) ) ;
#12350=DIRECTION ( 'NONE',  ( 1.000000000000000000, 0.000000000000000000, 0.000000000000000000 ) ) ;
#12356=VERTEX_POINT ( 'NONE', #2751 ) ;
#12360=ORIENTED_EDGE ( 'NONE', *, *, #11454, .T. ) ;
#12364=ORIENTED_EDGE ( 'NONE', *, *, #6995, .F. ) ;
#12393=PRODUCT ( 'hex bolt gradeab_iso_ISO 4014 - M5 x 30 x 16-N', 'hex bolt gradeab_iso_ISO 4014 - M5 x 30 x 16-N', '', ( #9757 ) ) ;
#12432=ORIENTED_EDGE ( 'NONE', *, *, #5808, .F. ) ;
#12462=ORIENTED_EDGE ( 'NONE', *, *, #2670, .T. ) ;
#12539=LINE ( 'NONE', #10319, #194 ) ;
#12543=CARTESIAN_POINT ( 'NONE',  ( 0.000000000000000000, 0.000000000000000000, 0.000000000000000000 ) ) ;
#12556=DIRECTION ( 'NONE',  ( -1.000000000000000000, -0.000000000000000000, -0.000000000000000000 ) ) ;
#12576=LINE ( 'NONE', #7254, #3067 ) ;
#12589=ORIENTED_EDGE ( 'NONE', *, *, #9352, .T. ) ;
#12590=PLANE ( 'NONE',  #6185 ) ;
#12626=ORIENTED_EDGE ( 'NONE', *, *, #5594, .F. ) ;
#12639=ORIENTED_EDGE ( 'NONE', *, *, #3315, .T. ) ;
#12650=DIRECTION ( 'NONE',  ( -1.000000000000000000, -0.000000000000000000, -0.000000000000000000 ) ) ;
#12652=AXIS2_PLACEMENT_3D ( 'NONE', #7045, #9275, #3738 ) ;
#12739=DIRECTION ( 'NONE',  ( 0.000000000000000000, 0.000000000000000000, -1.000000000000000000 ) ) ;
#12767=DIRECTION ( 'NONE',  ( 0.000000000000000000, 1.224646799147353207E-16, 1.000000000000000000 ) ) ;
#12779=FACE_OUTER_BOUND ( 'NONE', #14044, .T. ) ;
#12787=DIRECTION ( 'NONE',  ( 0.000000000000000000, -1.000000000000000000, 1.314525273895018220E-15 ) ) ;
#12796=EDGE_CURVE ( 'NONE', #6863, #5856, #12853, .T. ) ;
#12801=B_SPLINE_CURVE_WITH_KNOTS ( 'NONE', 3,
 ( #6228, #13993, #4908, #5195, #11829, #7411 ),
 .UNSPECIFIED., .F., .F.,
 ( 4, 2, 4 ),
 ( 0.01471339550406853582, 0.01588188803547990399, 0.01705038056689127043 ),
 .UNSPECIFIED. ) ;
#12812=CARTESIAN_POINT ( 'NONE',  ( 0.000000000000000000, 0.000000000000000000, 0.000000000000000000 ) ) ;
#12831=ADVANCED_FACE ( 'NONE', ( #10642 ), #6339, .F. ) ;
#12832=EDGE_CURVE ( 'NONE', #1059, #4259, #3796, .T. ) ;
#12840=CARTESIAN_POINT ( 'NONE',  ( 2.999999999999999112, 4.000000000000000000, 0.000000000000000000 ) ) ;
#12843=PLANE ( 'NONE',  #6569 ) ;
#12853=LINE ( 'NONE', #9538, #420 ) ;
#12872=ORIENTED_EDGE ( 'NONE', *, *, #5103, .F. ) ;
#12874=CARTESIAN_POINT ( 'NONE',  ( 33.05499999999999972, 0.000000000000000000, 0.000000000000000000 ) ) ;
#12875=ORIENTED_EDGE ( 'NONE', *, *, #12796, .F. ) ;
#12877=FACE_OUTER_BOUND ( 'NONE', #15, .T. ) ;
#12908=FACE_OUTER_BOUND ( 'NONE', #8695, .T. ) ;
#12912=DIRECTION ( 'NONE',  ( 0.000000000000000000, -1.314525273895018220E-15, -1.000000000000000000 ) ) ;
#12940=DIRECTION ( 'NONE',  ( 1.000000000000000000, 0.000000000000000000, -0.000000000000000000 ) ) ;
#12958=ORIENTED_EDGE ( 'NONE', *, *, #3315, .F. ) ;
#12970=CONICAL_SURFACE ( 'NONE', #6134, 4.000000000000000000, 1.047197551196600296 ) ;
#12989=AXIS2_PLACEMENT_3D ( 'NONE', #8766, #7719, #14365 ) ;
#12992=AXIS2_PLACEMENT_3D ( 'NONE', #8703, #5169, #12995 ) ;
#12995=DIRECTION ( 'NONE',  ( 0.000000000000000000, 0.000000000000000000, 1.000000000000000000 ) ) ;
#13001=VECTOR ( 'NONE', #844, 1000.000000000000000 ) ;
#13025=( NAMED_UNIT ( * ) PLANE_ANGLE_UNIT ( ) SI_UNIT ( $, .RADIAN. ) );
#13027=EDGE_LOOP ( 'NONE', ( #10773, #10497, #8491 ) ) ;
#13030=ADVANCED_BREP_SHAPE_REPRESENTATION ( '', ( #2645, #9440 ), #5943 ) ;
#13054=CARTESIAN_POINT ( 'NONE',  ( 0.1391502195351409510, 4.241015250120811153, -0.6543461111163325628 ) ) ;
#13078=ADVANCED_FACE ( 'NONE', ( #7754 ), #6805, .T. ) ;
#13080=DIRECTION ( 'NONE',  ( 0.000000000000000000, -0.5000000000000009992, 0.8660254037844381525 ) ) ;
#13090=DIRECTION ( 'NONE',  ( -1.000000000000000000, -0.000000000000000000, -0.000000000000000000 ) ) ;
#13118=ORIENTED_EDGE ( 'NONE', *, *, #10230, .T. ) ;
#13128=DIRECTION ( 'NONE',  ( 0.000000000000000000, 1.000000000000000000, -1.314525273895018220E-15 ) ) ;
#13147=VERTEX_POINT ( 'NONE', #4044 ) ;
#13156=DIRECTION ( 'NONE',  ( -0.7071067811865474617, 0.000000000000000000, 0.7071067811865474617 ) ) ;
#13181=ORIENTED_EDGE ( 'NONE', *, *, #10009, .T. ) ;
#13203=ORIENTED_EDGE ( 'NONE', *, *, #2101, .T. ) ;
#13224=LINE ( 'NONE', #2059, #9614 ) ;
#13240=( LENGTH_UNIT ( ) NAMED_UNIT ( * ) SI_UNIT ( .MILLI., .METRE. ) );
#13258=CARTESIAN_POINT ( 'NONE',  ( 0.000000000000000000, 3.464101615137751278, -2.000000000000006217 ) ) ;
#13276=VERTEX_POINT ( 'NONE', #2970 ) ;
#13287=DIRECTION ( 'NONE',  ( 1.000000000000000000, 0.000000000000000000, 0.000000000000000000 ) ) ;
#13298=CARTESIAN_POINT ( 'NONE',  ( 3.500000000000000000, 4.618802153517012954, 6.505213034913018715E-16 ) ) ;
#13299=EDGE_LOOP ( 'NONE', ( #4921, #7558, #1533, #1024, #4035, #5344 ) ) ;
#13322=CARTESIAN_POINT ( 'NONE',  ( 3.500000000000000000, 0.000000000000000000, 4.000000000000000000 ) ) ;
#13374=VERTEX_POINT ( 'NONE', #14374 ) ;
#13423=DIRECTION ( 'NONE',  ( 0.000000000000000000, -0.5000000000000009992, 0.8660254037844381525 ) ) ;
#13426=CARTESIAN_POINT ( 'NONE',  ( 0.2494252716035025574, 1.935831255942362494, -4.000000000000000000 ) ) ;
#13433=CIRCLE ( 'NONE', #468, 2.500000000000000444 ) ;
#13458=ORIENTED_EDGE ( 'NONE', *, *, #8850, .T. ) ;
#13461=AXIS2_PLACEMENT_3D ( 'NONE', #14512, #4401, #7582 ) ;
#13462=LINE ( 'NONE', #3357, #10583 ) ;
#13463=CIRCLE ( 'NONE', #12992, 4.000000000000000000 ) ;
#13466=EDGE_CURVE ( 'NONE', #13276, #2544, #4344, .T. ) ;
#13469=DIRECTION ( 'NONE',  ( 0.000000000000000000, -1.000000000000000000, 0.000000000000000000 ) ) ;
#13497=VECTOR ( 'NONE', #2818, 1000.000000000000000 ) ;
#13560=ORIENTED_EDGE ( 'NONE', *, *, #10230, .F. ) ;
#13567=CARTESIAN_POINT ( 'NONE',  ( 0.2484800633749957022, -4.430380094434235971, -0.3263565795980920559 ) ) ;
#13573=DIRECTION ( 'NONE',  ( 0.000000000000000000, 0.000000000000000000, 1.000000000000000000 ) ) ;
#13599=PLANE ( 'NONE',  #10862 ) ;
#13639=CIRCLE ( 'NONE', #10825, 4.000000000000000000 ) ;
#13651=DIRECTION ( 'NONE',  ( 0.000000000000000000, 0.000000000000000000, -1.000000000000000000 ) ) ;
#13718=VERTEX_POINT ( 'NONE', #9056 ) ;
#13725=ORIENTED_EDGE ( 'NONE', *, *, #4345, .F. ) ;
#13792=EDGE_CURVE ( 'NONE', #2766, #3675, #705, .T. ) ;
#13805=ORIENTED_EDGE ( 'NONE', *, *, #2581, .T. ) ;
#13810=CARTESIAN_POINT ( 'NONE',  ( 0.000000000000000000, 5.258101095580073669E-15, 4.000000000000000000 ) ) ;
#13833=EDGE_LOOP ( 'NONE', ( #5727, #5860, #9338 ) ) ;
#13836=CARTESIAN_POINT ( 'NONE',  ( 2.999999999999999112, 0.000000000000000000, 4.000000000000000000 ) ) ;
#13895=CARTESIAN_POINT ( 'NONE',  ( 2.999999999999999112, 2.309401076758508253, 3.999999999999993339 ) ) ;
#13916=ORIENTED_EDGE ( 'NONE', *, *, #12832, .F. ) ;
#13930=DIRECTION ( 'NONE',  ( 1.000000000000000000, 0.000000000000000000, -0.000000000000000000 ) ) ;
#13934=ORIENTED_EDGE ( 'NONE', *, *, #4778, .F. ) ;
#13938=AXIS2_PLACEMENT_3D ( 'NONE', #6944, #12556, #4820 ) ;
#13940=EDGE_CURVE ( 'NONE', #2544, #3675, #9851, .T. ) ;
#13967=CARTESIAN_POINT ( 'NONE',  ( 2.999999999999999112, 2.309401076758500704, -4.000000000000000000 ) ) ;
#13971=ADVANCED_FACE ( 'NONE', ( #2169 ), #12970, .T. ) ;
#13980=DIRECTION ( 'NONE',  ( 0.000000000000000000, 0.000000000000000000, -1.000000000000000000 ) ) ;
#13989=DIRECTION ( 'NONE',  ( -1.000000000000000000, -0.000000000000000000, -0.000000000000000000 ) ) ;
#13993=CARTESIAN_POINT ( 'NONE',  ( -1.143494478793305150E-17, -0.3908539631446752427, -4.000000000000000000 ) ) ;
#14001=DIRECTION ( 'NONE',  ( 0.000000000000000000, 0.000000000000000000, -1.000000000000000000 ) ) ;
#14003=DIRECTION ( 'NONE',  ( -1.000000000000000000, 0.000000000000000000, -0.000000000000000000 ) ) ;
#14017=LINE ( 'NONE', #14297, #5930 ) ;
#14028=DIRECTION ( 'NONE',  ( 0.000000000000000000, 0.000000000000000000, -1.000000000000000000 ) ) ;
#14040=CARTESIAN_POINT ( 'NONE',  ( 2.999999999999999112, 4.618802153517012954, 0.000000000000000000 ) ) ;
#14041=CARTESIAN_POINT ( 'NONE',  ( 0.000000000000000000, 3.464101615137751278, -2.000000000000006217 ) ) ;
#14044=EDGE_LOOP ( 'NONE', ( #12639, #8582, #13203 ) ) ;
#14062=LINE ( 'NONE', #3947, #12049 ) ;
#14098=EDGE_CURVE ( 'NONE', #3675, #10367, #10852, .T. ) ;
#14102=CIRCLE ( 'NONE', #1130, 4.000000000000000000 ) ;
#14111=LINE ( 'NONE', #295, #13497 ) ;
#14117=ORIENTED_EDGE ( 'NONE', *, *, #13792, .T. ) ;
#14155=AXIS2_PLACEMENT_3D ( 'NONE', #8962, #13469, #7867 ) ;
#14173=VECTOR ( 'NONE', #1549, 1000.000000000000114 ) ;
#14176=CARTESIAN_POINT ( 'NONE',  ( 2.999999999999999112, 0.000000000000000000, 0.000000000000000000 ) ) ;
#14177=EDGE_CURVE ( 'NONE', #14270, #4614, #12576, .T. ) ;
#14181=CARTESIAN_POINT ( 'NONE',  ( 3.500000000000000000, -4.618802153516999631, 0.000000000000000000 ) ) ;
#14183=UNCERTAINTY_MEASURE_WITH_UNIT (LENGTH_MEASURE( 1.000000000000000082E-05 ), #13240, 'distance_accuracy_value', 'NONE');
#14185=ORIENTED_EDGE ( 'NONE', *, *, #8539, .T. ) ;
#14204=DIRECTION ( 'NONE',  ( 1.000000000000000000, 0.000000000000000000, -0.000000000000000000 ) ) ;
#14222=CARTESIAN_POINT ( 'NONE',  ( 0.000000000000000000, 0.000000000000000000, 0.000000000000000000 ) ) ;
#14226=ORIENTED_EDGE ( 'NONE', *, *, #8539, .F. ) ;
#14230=ORIENTED_EDGE ( 'NONE', *, *, #10181, .T. ) ;
#14248=EDGE_CURVE ( 'NONE', #13718, #12356, #11490, .T. ) ;
#14255=ORIENTED_EDGE ( 'NONE', *, *, #8744, .T. ) ;
#14257=CARTESIAN_POINT ( 'NONE',  ( 0.03421028094653150164, 3.072372537026367478, -2.678494666091042475 ) ) ;
#14259=LINE ( 'NONE', #9894, #479 ) ;
#14270=VERTEX_POINT ( 'NONE', #10877 ) ;
#14297=CARTESIAN_POINT ( 'NONE',  ( 2.999999999999999112, -2.309401076758502480, -4.000000000000000000 ) ) ;
#14298=ORIENTED_EDGE ( 'NONE', *, *, #5808, .T. ) ;
#14302=DIRECTION ( 'NONE',  ( 0.000000000000000000, 0.000000000000000000, 1.000000000000000000 ) ) ;
#14308=CARTESIAN_POINT ( 'NONE',  ( 0.000000000000000000, 3.464101615137752610, 2.000000000000003997 ) ) ;
#14322=B_SPLINE_CURVE_WITH_KNOTS ( 'NONE', 3,
 ( #3559, #11587, #9311, #9153 ),
 .UNSPECIFIED., .F., .F.,
 ( 4, 4 ),
 ( 2.380737581618690687E-07, 0.002336974151641533874 ),
 .UNSPECIFIED. ) ;
#14335=ORIENTED_EDGE ( 'NONE', *, *, #13466, .T. ) ;
#14358=AXIS2_PLACEMENT_3D ( 'NONE', #6888, #3490, #10132 ) ;
#14365=DIRECTION ( 'NONE',  ( 0.000000000000000000, 0.000000000000000000, -1.000000000000000000 ) ) ;
#14374=CARTESIAN_POINT ( 'NONE',  ( 33.05499999999999972, 0.000000000000000000, 2.500000000000000444 ) ) ;
#14393=DIRECTION ( 'NONE',  ( -0.000000000000000000, 0.8660254037844391517, 0.4999999999999990563 ) ) ;
#14495=DIRECTION ( 'NONE',  ( -1.000000000000000000, -0.000000000000000000, -0.000000000000000000 ) ) ;
#14512=CARTESIAN_POINT ( 'NONE',  ( 2.999999999999999112, 4.000000000000000000, 0.000000000000000000 ) ) ;
#14525=ORIENTED_EDGE ( 'NONE', *, *, #6101, .F. ) ;
#14544=ADVANCED_FACE ( 'NONE', ( #1473 ), #11317, .T. ) ;
#14585=LINE ( 'NONE', #12292, #13001 ) ;
#14606=EDGE_CURVE ( 'NONE', #1758, #808, #3977, .T. ) ;
#14612=CARTESIAN_POINT ( 'NONE',  ( 0.000000000000000000, -3.464101615137757051, -1.999999999999996225 ) ) ;
#14675=COLOUR_RGB('Black',0.12,0.14,0.17);
#14676=FILL_AREA_STYLE_COLOUR('',#14675);
#14677=FILL_AREA_STYLE('',(#14676));
#14678=SURFACE_STYLE_FILL_AREA(#14677);
#14679=SURFACE_SIDE_STYLE('',(#14678));
#14680=SURFACE_STYLE_USAGE(.BOTH.,#14679);
#14681=PRESENTATION_STYLE_ASSIGNMENT((#14680));
ENDSEC;
END-ISO-10303-21;
